ISO-10303-21;
HEADER;
FILE_DESCRIPTION (('STEP AP214'),
    '1' );
FILE_NAME ('Part1.step',
    '2026-11-01T05:08:46',
    ( '' ),
    ( '' ),
    'SwSTEP 2.0',
    'SolidWorks 2024',
    '' );
FILE_SCHEMA (( 'AUTOMOTIVE_DESIGN' ));
ENDSEC;

DATA;
#3=ORIENTED_EDGE ( 'NONE', *, *, #13457, .T. ) ;
#39=ORIENTED_EDGE ( 'NONE', *, *, #11105, .T. ) ;
#47=LINE ( 'NONE', #6217, #13812 ) ;
#150=EDGE_CURVE ( 'NONE', #6128, #3161, #9700, .T. ) ;
#156=DIRECTION ( 'NONE',  ( 0.000000000000000000, 0.000000000000000000, 1.000000000000000000 ) ) ;
#183=UNCERTAINTY_MEASURE_WITH_UNIT (LENGTH_MEASURE( 1.000000000000000082E-05 ), #16217, 'distance_accuracy_value', 'NONE');
#202=AXIS2_PLACEMENT_3D ( 'NONE', #7053, #629, #9652 ) ;
#208=ORIENTED_EDGE ( 'NONE', *, *, #16440, .T. ) ;
#269=PLANE ( 'NONE',  #5082 ) ;
#297=ORIENTED_EDGE ( 'NONE', *, *, #9912, .F. ) ;
#301=FACE_BOUND ( 'NONE', #15224, .T. ) ;
#338=EDGE_LOOP ( 'NONE', ( #11132, #6961, #8646, #13596 ) ) ;
#344=DIRECTION ( 'NONE',  ( -1.000000000000000000, -0.000000000000000000, -1.631319816340925608E-17 ) ) ;
#368=ORIENTED_EDGE ( 'NONE', *, *, #11512, .F. ) ;
#377=VERTEX_POINT ( 'NONE', #14230 ) ;
#402=DIRECTION ( 'NONE',  ( -0.000000000000000000, -1.000000000000000000, -0.000000000000000000 ) ) ;
#461=CARTESIAN_POINT ( 'NONE',  ( 64.99999999999998579, 0.000000000000000000, -17.00000000000000355 ) ) ;
#464=ORIENTED_EDGE ( 'NONE', *, *, #15230, .F. ) ;
#475=DIRECTION ( 'NONE',  ( 1.000000000000000000, 0.000000000000000000, 0.000000000000000000 ) ) ;
#476=EDGE_CURVE ( 'NONE', #15129, #9524, #13514, .T. ) ;
#478=VERTEX_POINT ( 'NONE', #11649 ) ;
#509=EDGE_LOOP ( 'NONE', ( #15845, #8645 ) ) ;
#552=ORIENTED_EDGE ( 'NONE', *, *, #4766, .T. ) ;
#580=LINE ( 'NONE', #5728, #7140 ) ;
#629=DIRECTION ( 'NONE',  ( -0.000000000000000000, 1.000000000000000000, -0.000000000000000000 ) ) ;
#669=CARTESIAN_POINT ( 'NONE',  ( 27.49999999999999645, 196.3050121726289206, -75.00000000000000000 ) ) ;
#688=VECTOR ( 'NONE', #12772, 1000.000000000000000 ) ;
#698=ORIENTED_EDGE ( 'NONE', *, *, #4584, .F. ) ;
#743=CARTESIAN_POINT ( 'NONE',  ( 47.50000000000000000, 196.3050121726289206, -17.00000000000000000 ) ) ;
#795=CARTESIAN_POINT ( 'NONE',  ( 0.000000000000000000, 380.0000000000000000, 0.000000000000000000 ) ) ;
#807=ADVANCED_FACE ( 'NONE', ( #12835, #7494 ), #16771, .F. ) ;
#826=ORIENTED_EDGE ( 'NONE', *, *, #12976, .T. ) ;
#862=CARTESIAN_POINT ( 'NONE',  ( 37.18009836720079875, 352.3758082234937206, -75.00000000000000000 ) ) ;
#882=VERTEX_POINT ( 'NONE', #7838 ) ;
#940=DIRECTION ( 'NONE',  ( -0.000000000000000000, -1.000000000000000000, 0.000000000000000000 ) ) ;
#952=CARTESIAN_POINT ( 'NONE',  ( 6.117449311278481738E-17, 277.8092731128509740, -44.71049682360898458 ) ) ;
#976=VERTEX_POINT ( 'NONE', #4338 ) ;
#1013=CYLINDRICAL_SURFACE ( 'NONE', #16824, 7.500000000000000000 ) ;
#1071=APPLICATION_CONTEXT ( 'automotive_design' ) ;
#1072=FACE_OUTER_BOUND ( 'NONE', #11758, .T. ) ;
#1078=ORIENTED_EDGE ( 'NONE', *, *, #11191, .F. ) ;
#1081=LINE ( 'NONE', #10437, #5575 ) ;
#1083=CARTESIAN_POINT ( 'NONE',  ( 0.000000000000000000, 0.000000000000000000, 0.000000000000000000 ) ) ;
#1114=AXIS2_PLACEMENT_3D ( 'NONE', #5436, #4250, #9490 ) ;
#1138=CLOSED_SHELL ( 'NONE', ( #15165, #6252, #9269, #4888, #3658, #807, #7631, #15966, #10966, #11049, #10661, #15869, #8338, #5630, #9841, #4327, #3632, #5285, #1796, #13193 ) ) ;
#1163=CARTESIAN_POINT ( 'NONE',  ( 17.00000000000000711, 380.0000000000000000, -17.00000000000000355 ) ) ;
#1205=CARTESIAN_POINT ( 'NONE',  ( 29.68009836720079875, 275.4439001176564830, -75.00000000000000000 ) ) ;
#1220=EDGE_LOOP ( 'NONE', ( #12300, #2857, #7476, #5756 ) ) ;
#1227=EDGE_CURVE ( 'NONE', #2521, #15829, #12875, .T. ) ;
#1246=ORIENTED_EDGE ( 'NONE', *, *, #9827, .F. ) ;
#1255=DIRECTION ( 'NONE',  ( -1.631319816340925300E-17, -0.000000000000000000, 1.000000000000000000 ) ) ;
#1259=FACE_BOUND ( 'NONE', #12186, .T. ) ;
#1287=CIRCLE ( 'NONE', #14740, 10.00000000000000178 ) ;
#1329=SHAPE_REPRESENTATION ( 'Part1', ( #1488 ), #8346 ) ;
#1347=CARTESIAN_POINT ( 'NONE',  ( 17.00000000000000355, 277.8092731128509740, -44.71049682360899169 ) ) ;
#1374=CARTESIAN_POINT ( 'NONE',  ( 44.68009836720081296, 275.4439001176564830, -75.00000000000000000 ) ) ;
#1413=LINE ( 'NONE', #6379, #1689 ) ;
#1426=PLANE ( 'NONE',  #10886 ) ;
#1430=ORIENTED_EDGE ( 'NONE', *, *, #150, .F. ) ;
#1431=AXIS2_PLACEMENT_3D ( 'NONE', #2052, #8588, #12449 ) ;
#1459=VERTEX_POINT ( 'NONE', #1163 ) ;
#1463=DIRECTION ( 'NONE',  ( 0.000000000000000000, -1.000000000000000000, 0.000000000000000000 ) ) ;
#1468=CYLINDRICAL_SURFACE ( 'NONE', #10100, 7.500000000000003553 ) ;
#1488=AXIS2_PLACEMENT_3D ( 'NONE', #3280, #8693, #15217 ) ;
#1513=PRODUCT ( 'Part1', 'Part1', '', ( #12628 ) ) ;
#1564=ORIENTED_EDGE ( 'NONE', *, *, #10984, .F. ) ;
#1571=ORIENTED_EDGE ( 'NONE', *, *, #9411, .T. ) ;
#1629=VERTEX_POINT ( 'NONE', #14992 ) ;
#1689=VECTOR ( 'NONE', #12922, 1000.000000000000000 ) ;
#1701=CARTESIAN_POINT ( 'NONE',  ( 44.68009836720079875, 352.3758082234937206, 0.000000000000000000 ) ) ;
#1707=VECTOR ( 'NONE', #2650, 1000.000000000000000 ) ;
#1727=DIRECTION ( 'NONE',  ( -1.000000000000000000, 0.000000000000000000, 0.000000000000000000 ) ) ;
#1741=ORIENTED_EDGE ( 'NONE', *, *, #13457, .F. ) ;
#1761=VECTOR ( 'NONE', #12386, 1000.000000000000000 ) ;
#1763=DIRECTION ( 'NONE',  ( 0.000000000000000000, 0.000000000000000000, 1.000000000000000000 ) ) ;
#1796=ADVANCED_FACE ( 'NONE', ( #11951 ), #1468, .F. ) ;
#1854=EDGE_CURVE ( 'NONE', #3376, #11568, #3252, .T. ) ;
#1898=VECTOR ( 'NONE', #402, 1000.000000000000000 ) ;
#1904=ORIENTED_EDGE ( 'NONE', *, *, #7512, .T. ) ;
#1909=ORIENTED_EDGE ( 'NONE', *, *, #12976, .F. ) ;
#1979=FACE_OUTER_BOUND ( 'NONE', #16392, .T. ) ;
#1990=ORIENTED_EDGE ( 'NONE', *, *, #11512, .T. ) ;
#1991=CIRCLE ( 'NONE', #2538, 7.500000000000000000 ) ;
#1998=EDGE_CURVE ( 'NONE', #15577, #2365, #12290, .T. ) ;
#2052=CARTESIAN_POINT ( 'NONE',  ( 7.000000000000001776, 380.0000000000000000, -65.00000000000000000 ) ) ;
#2070=DIRECTION ( 'NONE',  ( -0.000000000000000000, -1.000000000000000000, -0.000000000000000000 ) ) ;
#2080=EDGE_CURVE ( 'NONE', #5021, #4345, #3601, .T. ) ;
#2104=EDGE_LOOP ( 'NONE', ( #4360, #15232, #4965, #16382 ) ) ;
#2113=LINE ( 'NONE', #12593, #14387 ) ;
#2176=LINE ( 'NONE', #6275, #6647 ) ;
#2190=VECTOR ( 'NONE', #1255, 1000.000000000000000 ) ;
#2288=DIRECTION ( 'NONE',  ( 0.000000000000000000, 0.000000000000000000, -1.000000000000000000 ) ) ;
#2359=DIRECTION ( 'NONE',  ( -1.000000000000000000, -0.000000000000000000, -0.000000000000000000 ) ) ;
#2365=VERTEX_POINT ( 'NONE', #13783 ) ;
#2397=ORIENTED_EDGE ( 'NONE', *, *, #6460, .T. ) ;
#2408=ORIENTED_EDGE ( 'NONE', *, *, #4465, .T. ) ;
#2518=AXIS2_PLACEMENT_3D ( 'NONE', #4012, #2288, #15430 ) ;
#2521=VERTEX_POINT ( 'NONE', #14285 ) ;
#2522=PLANE ( 'NONE',  #9479 ) ;
#2530=ORIENTED_EDGE ( 'NONE', *, *, #13582, .F. ) ;
#2538=AXIS2_PLACEMENT_3D ( 'NONE', #9525, #13475, #6832 ) ;
#2562=DIRECTION ( 'NONE',  ( -0.000000000000000000, -0.000000000000000000, 1.000000000000000000 ) ) ;
#2583=DIRECTION ( 'NONE',  ( -0.000000000000000000, -0.000000000000000000, 1.000000000000000000 ) ) ;
#2593=ORIENTED_EDGE ( 'NONE', *, *, #2675, .T. ) ;
#2599=ORIENTED_EDGE ( 'NONE', *, *, #2080, .F. ) ;
#2634=VECTOR ( 'NONE', #2562, 1000.000000000000000 ) ;
#2650=DIRECTION ( 'NONE',  ( 0.000000000000000000, 0.000000000000000000, -1.000000000000000000 ) ) ;
#2664=DIRECTION ( 'NONE',  ( -1.000000000000000000, -0.000000000000000000, -1.631319816340925608E-17 ) ) ;
#2675=EDGE_CURVE ( 'NONE', #1629, #8468, #8037, .T. ) ;
#2705=DIRECTION ( 'NONE',  ( 0.000000000000000000, 0.000000000000000000, -1.000000000000000000 ) ) ;
#2744=UNCERTAINTY_MEASURE_WITH_UNIT (LENGTH_MEASURE( 1.000000000000000082E-05 ), #7740, 'distance_accuracy_value', 'NONE');
#2754=VECTOR ( 'NONE', #16109, 1000.000000000000000 ) ;
#2843=DIRECTION ( 'NONE',  ( 0.000000000000000000, 0.000000000000000000, -1.000000000000000000 ) ) ;
#2849=ORIENTED_EDGE ( 'NONE', *, *, #150, .T. ) ;
#2857=ORIENTED_EDGE ( 'NONE', *, *, #9913, .T. ) ;
#2877=CIRCLE ( 'NONE', #8087, 10.00000000000000178 ) ;
#2889=FACE_OUTER_BOUND ( 'NONE', #11361, .T. ) ;
#2907=DIRECTION ( 'NONE',  ( -1.071014023499572265E-32, 1.000000000000000000, -8.952264470854156086E-17 ) ) ;
#2961=EDGE_LOOP ( 'NONE', ( #6567, #464, #297, #14177 ) ) ;
#2997=CARTESIAN_POINT ( 'NONE',  ( 29.68009836720079875, 352.3758082234937206, -17.00000000000000000 ) ) ;
#3000=DIRECTION ( 'NONE',  ( 1.000000000000000000, 0.000000000000000000, 0.000000000000000000 ) ) ;
#3013=DIRECTION ( 'NONE',  ( -1.000000000000000000, -0.000000000000000000, -1.631319816340925608E-17 ) ) ;
#3018=EDGE_CURVE ( 'NONE', #9524, #15129, #16298, .T. ) ;
#3040=DIRECTION ( 'NONE',  ( -0.000000000000000000, -0.000000000000000000, 1.000000000000000000 ) ) ;
#3073=ORIENTED_EDGE ( 'NONE', *, *, #16355, .F. ) ;
#3089=CARTESIAN_POINT ( 'NONE',  ( 75.00000000000000000, 277.8092731128509740, -29.71049682360898103 ) ) ;
#3093=VERTEX_POINT ( 'NONE', #5755 ) ;
#3141=CARTESIAN_POINT ( 'NONE',  ( 17.00000000000000000, 355.3192028797624857, -44.71049682360899169 ) ) ;
#3146=CARTESIAN_POINT ( 'NONE',  ( 29.68009836720079875, 275.4439001176565398, -17.00000000000000355 ) ) ;
#3155=DIRECTION ( 'NONE',  ( -0.000000000000000000, 1.000000000000000000, -0.000000000000000000 ) ) ;
#3161=VERTEX_POINT ( 'NONE', #15209 ) ;
#3173=CIRCLE ( 'NONE', #10838, 7.500000000000003553 ) ;
#3182=EDGE_LOOP ( 'NONE', ( #9359, #13565, #7138, #11443 ) ) ;
#3252=CIRCLE ( 'NONE', #7347, 7.500000000000000000 ) ;
#3263=LINE ( 'NONE', #11161, #3921 ) ;
#3280=CARTESIAN_POINT ( 'NONE',  ( 0.000000000000000000, 0.000000000000000000, 0.000000000000000000 ) ) ;
#3321=CARTESIAN_POINT ( 'NONE',  ( 37.18009836720080585, 275.4439001176564830, -75.00000000000000000 ) ) ;
#3325=VECTOR ( 'NONE', #10889, 1000.000000000000000 ) ;
#3326=EDGE_CURVE ( 'NONE', #1459, #3093, #5564, .T. ) ;
#3329=DIRECTION ( 'NONE',  ( -0.000000000000000000, -0.000000000000000000, 1.000000000000000000 ) ) ;
#3359=ORIENTED_EDGE ( 'NONE', *, *, #7512, .F. ) ;
#3364=LINE ( 'NONE', #7124, #10139 ) ;
#3376=VERTEX_POINT ( 'NONE', #9270 ) ;
#3414=DIRECTION ( 'NONE',  ( 1.631319816340925608E-17, 0.000000000000000000, -1.000000000000000000 ) ) ;
#3416=ORIENTED_EDGE ( 'NONE', *, *, #16440, .F. ) ;
#3418=AXIS2_PLACEMENT_3D ( 'NONE', #795, #7049, #16339 ) ;
#3446=EDGE_CURVE ( 'NONE', #7810, #9725, #2877, .T. ) ;
#3450=CIRCLE ( 'NONE', #5636, 7.500000000000000000 ) ;
#3459=CIRCLE ( 'NONE', #12785, 7.500000000000007105 ) ;
#3507=DIRECTION ( 'NONE',  ( 0.000000000000000000, 0.000000000000000000, 1.000000000000000000 ) ) ;
#3515=CYLINDRICAL_SURFACE ( 'NONE', #1431, 9.999999999999994671 ) ;
#3541=ORIENTED_EDGE ( 'NONE', *, *, #1854, .T. ) ;
#3601=LINE ( 'NONE', #4883, #6517 ) ;
#3625=EDGE_CURVE ( 'NONE', #1459, #6709, #14062, .T. ) ;
#3632=ADVANCED_FACE ( 'NONE', ( #14232 ), #1013, .F. ) ;
#3658=ADVANCED_FACE ( 'NONE', ( #1259, #9165, #2889 ), #5454, .F. ) ;
#3666=ORIENTED_EDGE ( 'NONE', *, *, #13074, .T. ) ;
#3699=CARTESIAN_POINT ( 'NONE',  ( 17.00000000000000711, 277.8092731128509740, -37.21049682360897748 ) ) ;
#3861=VECTOR ( 'NONE', #2359, 1000.000000000000000 ) ;
#3921=VECTOR ( 'NONE', #7190, 1000.000000000000000 ) ;
#3940=EDGE_LOOP ( 'NONE', ( #3073, #16399, #7334, #7666 ) ) ;
#3948=DIRECTION ( 'NONE',  ( -1.196361017915039486E-16, -0.000000000000000000, -1.000000000000000000 ) ) ;
#3979=EDGE_LOOP ( 'NONE', ( #2599, #12838, #10560, #11598 ) ) ;
#4012=CARTESIAN_POINT ( 'NONE',  ( 37.50000000000000000, 196.3050121726289206, 0.000000000000000000 ) ) ;
#4104=VECTOR ( 'NONE', #13845, 1000.000000000000000 ) ;
#4108=DIRECTION ( 'NONE',  ( -1.803905316987902281E-16, 1.000000000000000000, 0.000000000000000000 ) ) ;
#4157=CARTESIAN_POINT ( 'NONE',  ( 0.000000000000000000, 277.8092731128509740, -37.21049682360897748 ) ) ;
#4167=EDGE_LOOP ( 'NONE', ( #3416, #13825, #12066, #7218 ) ) ;
#4194=LINE ( 'NONE', #14682, #9802 ) ;
#4218=CARTESIAN_POINT ( 'NONE',  ( 75.00000000000000000, 277.8092731128509740, -37.21049682360897748 ) ) ;
#4250=DIRECTION ( 'NONE',  ( 0.000000000000000000, 0.000000000000000000, -1.000000000000000000 ) ) ;
#4274=AXIS2_PLACEMENT_3D ( 'NONE', #12692, #5194, #3507 ) ;
#4303=LINE ( 'NONE', #3089, #9463 ) ;
#4312=CIRCLE ( 'NONE', #202, 9.999999999999994671 ) ;
#4327=ADVANCED_FACE ( 'NONE', ( #1979 ), #7205, .F. ) ;
#4338=CARTESIAN_POINT ( 'NONE',  ( 7.000000000000001776, 380.0000000000000000, -75.00000000000000000 ) ) ;
#4345=VERTEX_POINT ( 'NONE', #952 ) ;
#4360=ORIENTED_EDGE ( 'NONE', *, *, #7797, .F. ) ;
#4408=DIRECTION ( 'NONE',  ( -0.000000000000000000, -0.000000000000000000, 1.000000000000000000 ) ) ;
#4452=AXIS2_PLACEMENT_3D ( 'NONE', #13231, #1463, #11946 ) ;
#4465=EDGE_CURVE ( 'NONE', #5021, #882, #3173, .T. ) ;
#4531=CARTESIAN_POINT ( 'NONE',  ( 1.223489862255693833E-15, 0.000000000000000000, -75.00000000000000000 ) ) ;
#4552=ORIENTED_EDGE ( 'NONE', *, *, #7797, .T. ) ;
#4553=DIRECTION ( 'NONE',  ( -0.000000000000000000, -1.000000000000000000, -0.000000000000000000 ) ) ;
#4584=EDGE_CURVE ( 'NONE', #9725, #7810, #6159, .T. ) ;
#4587=VERTEX_POINT ( 'NONE', #10561 ) ;
#4625=LINE ( 'NONE', #15281, #7729 ) ;
#4718=DIRECTION ( 'NONE',  ( -0.000000000000000000, 0.000000000000000000, 1.000000000000000000 ) ) ;
#4724=DIRECTION ( 'NONE',  ( 0.000000000000000000, 0.000000000000000000, -1.000000000000000000 ) ) ;
#4766=EDGE_CURVE ( 'NONE', #478, #5489, #13573, .T. ) ;
#4793=EDGE_CURVE ( 'NONE', #12485, #3376, #10375, .T. ) ;
#4883=CARTESIAN_POINT ( 'NONE',  ( 75.00000000000000000, 277.8092731128509740, -44.71049682360897748 ) ) ;
#4888=ADVANCED_FACE ( 'NONE', ( #13982 ), #6233, .F. ) ;
#4944=DIRECTION ( 'NONE',  ( 0.000000000000000000, 0.000000000000000000, 1.000000000000000000 ) ) ;
#4961=AXIS2_PLACEMENT_3D ( 'NONE', #15515, #8986, #2705 ) ;
#4965=ORIENTED_EDGE ( 'NONE', *, *, #9411, .F. ) ;
#4977=EDGE_LOOP ( 'NONE', ( #12366, #7904, #8961, #5215 ) ) ;
#5020=CARTESIAN_POINT ( 'NONE',  ( 37.50000000000000000, 196.3050121726289206, -75.00000000000000000 ) ) ;
#5021=VERTEX_POINT ( 'NONE', #1347 ) ;
#5024=CARTESIAN_POINT ( 'NONE',  ( 75.00000000000000000, 355.3192028797624857, -29.71049682360898814 ) ) ;
#5043=PRODUCT_DEFINITION ( 'UNKNOWN', '', #11940, #6352 ) ;
#5056=EDGE_CURVE ( 'NONE', #9819, #5558, #3450, .T. ) ;
#5082=AXIS2_PLACEMENT_3D ( 'NONE', #12206, #5749, #9627 ) ;
#5139=STYLED_ITEM ( 'NONE', ( #7101 ), #8514 ) ;
#5185=CARTESIAN_POINT ( 'NONE',  ( 64.99999999999998579, 380.0000000000000000, -17.00000000000000355 ) ) ;
#5194=DIRECTION ( 'NONE',  ( -1.000000000000000000, 0.000000000000000000, 0.000000000000000000 ) ) ;
#5215=ORIENTED_EDGE ( 'NONE', *, *, #11384, .T. ) ;
#5285=ADVANCED_FACE ( 'NONE', ( #1072 ), #2522, .F. ) ;
#5302=ORIENTED_EDGE ( 'NONE', *, *, #9729, .T. ) ;
#5379=EDGE_CURVE ( 'NONE', #16667, #6128, #3459, .T. ) ;
#5436=CARTESIAN_POINT ( 'NONE',  ( 0.000000000000000000, 380.0000000000000000, 0.000000000000000000 ) ) ;
#5451=DIRECTION ( 'NONE',  ( 1.000000000000000000, 0.000000000000000000, -0.000000000000000000 ) ) ;
#5454=PLANE ( 'NONE',  #7227 ) ;
#5489=VERTEX_POINT ( 'NONE', #16008 ) ;
#5490=CIRCLE ( 'NONE', #12625, 7.500000000000003553 ) ;
#5518=FACE_BOUND ( 'NONE', #509, .T. ) ;
#5557=LINE ( 'NONE', #9264, #15262 ) ;
#5558=VERTEX_POINT ( 'NONE', #3141 ) ;
#5560=EDGE_CURVE ( 'NONE', #14313, #9254, #13059, .T. ) ;
#5564=LINE ( 'NONE', #7879, #9136 ) ;
#5575=VECTOR ( 'NONE', #15668, 1000.000000000000000 ) ;
#5588=CARTESIAN_POINT ( 'NONE',  ( 37.50000000000000000, 196.3050121726289206, 0.000000000000000000 ) ) ;
#5590=EDGE_LOOP ( 'NONE', ( #12670, #1564, #15806, #2849 ) ) ;
#5630=ADVANCED_FACE ( 'NONE', ( #7976 ), #269, .F. ) ;
#5636=AXIS2_PLACEMENT_3D ( 'NONE', #13298, #6654, #156 ) ;
#5643=LINE ( 'NONE', #10707, #3325 ) ;
#5728=CARTESIAN_POINT ( 'NONE',  ( 1.223489862255693833E-15, 380.0000000000000000, -75.00000000000000000 ) ) ;
#5737=CARTESIAN_POINT ( 'NONE',  ( 37.50000000000000000, 196.3050121726289206, -17.00000000000000000 ) ) ;
#5749=DIRECTION ( 'NONE',  ( 1.000000000000000000, 1.803905316987902281E-16, 0.000000000000000000 ) ) ;
#5755=CARTESIAN_POINT ( 'NONE',  ( 17.00000000000000000, 380.0000000000000000, -65.00000000000000000 ) ) ;
#5756=ORIENTED_EDGE ( 'NONE', *, *, #13051, .F. ) ;
#5825=VECTOR ( 'NONE', #8715, 1000.000000000000000 ) ;
#5853=CYLINDRICAL_SURFACE ( 'NONE', #12938, 10.00000000000000178 ) ;
#5854=FACE_OUTER_BOUND ( 'NONE', #9151, .T. ) ;
#5943=CARTESIAN_POINT ( 'NONE',  ( 65.00000000000000000, 380.0000000000000000, -17.00000000000000355 ) ) ;
#5954=ORIENTED_EDGE ( 'NONE', *, *, #16418, .F. ) ;
#5970=EDGE_LOOP ( 'NONE', ( #698, #208, #10419, #8954 ) ) ;
#6023=EDGE_CURVE ( 'NONE', #7810, #9524, #5557, .T. ) ;
#6118=CARTESIAN_POINT ( 'NONE',  ( 6.117449311278470645E-17, 355.3192028797624857, -44.71049682360899169 ) ) ;
#6128=VERTEX_POINT ( 'NONE', #7959 ) ;
#6135=CARTESIAN_POINT ( 'NONE',  ( 17.00000000000000711, 355.3192028797624857, -29.71049682360898814 ) ) ;
#6138=EDGE_CURVE ( 'NONE', #882, #9819, #4194, .T. ) ;
#6146=LINE ( 'NONE', #5024, #6289 ) ;
#6154=CARTESIAN_POINT ( 'NONE',  ( 0.000000000000000000, 355.3192028797624857, -29.71049682360898814 ) ) ;
#6159=CIRCLE ( 'NONE', #14402, 10.00000000000000178 ) ;
#6184=CARTESIAN_POINT ( 'NONE',  ( 17.00000000000000711, 0.000000000000000000, -17.00000000000000355 ) ) ;
#6217=CARTESIAN_POINT ( 'NONE',  ( 17.00000000000000000, 380.0000000000000000, -65.00000000000000000 ) ) ;
#6233=PLANE ( 'NONE',  #4274 ) ;
#6251=DIRECTION ( 'NONE',  ( -1.000000000000000000, 0.000000000000000000, 1.196361017915039732E-16 ) ) ;
#6252=ADVANCED_FACE ( 'NONE', ( #13647, #7094 ), #15013, .F. ) ;
#6275=CARTESIAN_POINT ( 'NONE',  ( 17.00000000000000000, 0.000000000000000000, -75.00000000000000000 ) ) ;
#6288=CARTESIAN_POINT ( 'NONE',  ( 75.00000000000000000, 355.3192028797624857, -29.71049682360898814 ) ) ;
#6289=VECTOR ( 'NONE', #10110, 1000.000000000000000 ) ;
#6297=CARTESIAN_POINT ( 'NONE',  ( 1.223489862255693833E-15, 380.0000000000000000, -75.00000000000000000 ) ) ;
#6326=CARTESIAN_POINT ( 'NONE',  ( 75.00000000000000000, 0.000000000000000000, 0.000000000000000000 ) ) ;
#6352=PRODUCT_DEFINITION_CONTEXT ( 'detailed design', #1071, 'design' ) ;
#6379=CARTESIAN_POINT ( 'NONE',  ( 7.000000000000001776, 380.0000000000000000, -75.00000000000000000 ) ) ;
#6400=AXIS2_PLACEMENT_3D ( 'NONE', #5588, #2843, #1727 ) ;
#6460=EDGE_CURVE ( 'NONE', #3093, #976, #4312, .T. ) ;
#6510=DIRECTION ( 'NONE',  ( 0.000000000000000000, -1.000000000000000000, 0.000000000000000000 ) ) ;
#6517=VECTOR ( 'NONE', #11417, 1000.000000000000000 ) ;
#6558=CARTESIAN_POINT ( 'NONE',  ( 1.223489862255693833E-15, 380.0000000000000000, -75.00000000000000000 ) ) ;
#6567=ORIENTED_EDGE ( 'NONE', *, *, #6460, .F. ) ;
#6647=VECTOR ( 'NONE', #7405, 1000.000000000000000 ) ;
#6654=DIRECTION ( 'NONE',  ( -1.000000000000000000, 0.000000000000000000, 1.196361017915039732E-16 ) ) ;
#6655=VECTOR ( 'NONE', #16543, 1000.000000000000000 ) ;
#6709=VERTEX_POINT ( 'NONE', #6184 ) ;
#6719=CARTESIAN_POINT ( 'NONE',  ( 37.18009836720079875, 352.3758082234937206, -17.00000000000000000 ) ) ;
#6724=DIRECTION ( 'NONE',  ( -1.631319816340925300E-17, 0.000000000000000000, 1.000000000000000000 ) ) ;
#6756=DIRECTION ( 'NONE',  ( -0.000000000000000000, -0.000000000000000000, 1.000000000000000000 ) ) ;
#6780=CARTESIAN_POINT ( 'NONE',  ( 0.000000000000000000, 355.3192028797624857, -37.21049682360899169 ) ) ;
#6807=VECTOR ( 'NONE', #4553, 1000.000000000000000 ) ;
#6832=DIRECTION ( 'NONE',  ( 1.000000000000000000, 0.000000000000000000, 0.000000000000000000 ) ) ;
#6842=( NAMED_UNIT ( * ) SI_UNIT ( $, .STERADIAN. ) SOLID_ANGLE_UNIT ( ) );
#6878=ORIENTED_EDGE ( 'NONE', *, *, #3326, .F. ) ;
#6961=ORIENTED_EDGE ( 'NONE', *, *, #5560, .F. ) ;
#6993=PRODUCT_DEFINITION_SHAPE ( 'NONE', 'NONE',  #5043 ) ;
#7049=DIRECTION ( 'NONE',  ( 0.000000000000000000, -1.000000000000000000, 0.000000000000000000 ) ) ;
#7053=CARTESIAN_POINT ( 'NONE',  ( 7.000000000000001776, 380.0000000000000000, -65.00000000000000000 ) ) ;
#7094=FACE_OUTER_BOUND ( 'NONE', #3182, .T. ) ;
#7101=PRESENTATION_STYLE_ASSIGNMENT (( #12017 ) ) ;
#7124=CARTESIAN_POINT ( 'NONE',  ( 75.00000000000000000, 380.0000000000000000, 0.000000000000000000 ) ) ;
#7138=ORIENTED_EDGE ( 'NONE', *, *, #13074, .F. ) ;
#7140=VECTOR ( 'NONE', #7163, 1000.000000000000000 ) ;
#7163=DIRECTION ( 'NONE',  ( -1.000000000000000000, -0.000000000000000000, -0.000000000000000000 ) ) ;
#7168=DIRECTION ( 'NONE',  ( 0.000000000000000000, -1.000000000000000000, 0.000000000000000000 ) ) ;
#7184=EDGE_CURVE ( 'NONE', #1629, #3161, #7537, .T. ) ;
#7190=DIRECTION ( 'NONE',  ( -0.000000000000000000, -0.000000000000000000, 1.000000000000000000 ) ) ;
#7205=PLANE ( 'NONE',  #16306 ) ;
#7211=AXIS2_PLACEMENT_3D ( 'NONE', #10421, #12911, #7746 ) ;
#7218=ORIENTED_EDGE ( 'NONE', *, *, #476, .F. ) ;
#7227=AXIS2_PLACEMENT_3D ( 'NONE', #11910, #14666, #10532 ) ;
#7260=LINE ( 'NONE', #16063, #688 ) ;
#7296=CARTESIAN_POINT ( 'NONE',  ( 29.68009836720079875, 352.3758082234937206, -75.00000000000000000 ) ) ;
#7305=CYLINDRICAL_SURFACE ( 'NONE', #11911, 10.00000000000000178 ) ;
#7334=ORIENTED_EDGE ( 'NONE', *, *, #4793, .F. ) ;
#7335=ORIENTED_EDGE ( 'NONE', *, *, #13997, .F. ) ;
#7340=CARTESIAN_POINT ( 'NONE',  ( 27.49999999999999645, 196.3050121726289206, 0.000000000000000000 ) ) ;
#7347=AXIS2_PLACEMENT_3D ( 'NONE', #6780, #2664, #10653 ) ;
#7405=DIRECTION ( 'NONE',  ( -1.196361017915039486E-16, -0.000000000000000000, -1.000000000000000000 ) ) ;
#7476=ORIENTED_EDGE ( 'NONE', *, *, #9827, .T. ) ;
#7494=FACE_OUTER_BOUND ( 'NONE', #11145, .T. ) ;
#7512=EDGE_CURVE ( 'NONE', #10513, #6709, #14153, .T. ) ;
#7537=LINE ( 'NONE', #10463, #2634 ) ;
#7542=EDGE_LOOP ( 'NONE', ( #10762, #8838, #14102, #12418 ) ) ;
#7631=ADVANCED_FACE ( 'NONE', ( #14827 ), #1426, .F. ) ;
#7666=ORIENTED_EDGE ( 'NONE', *, *, #9203, .F. ) ;
#7677=CARTESIAN_POINT ( 'NONE',  ( 17.00000000000000711, 0.000000000000000000, -17.00000000000000355 ) ) ;
#7705=ORIENTED_EDGE ( 'NONE', *, *, #9630, .T. ) ;
#7729=VECTOR ( 'NONE', #15200, 1000.000000000000000 ) ;
#7740=( LENGTH_UNIT ( ) NAMED_UNIT ( * ) SI_UNIT ( .MILLI., .METRE. ) );
#7746=DIRECTION ( 'NONE',  ( 1.196361017915039732E-16, 0.000000000000000000, 1.000000000000000000 ) ) ;
#7751=DIRECTION ( 'NONE',  ( 0.000000000000000000, -1.000000000000000000, 8.952264470854156086E-17 ) ) ;
#7796=ORIENTED_EDGE ( 'NONE', *, *, #6138, .T. ) ;
#7797=EDGE_CURVE ( 'NONE', #5489, #16470, #1287, .T. ) ;
#7810=VERTEX_POINT ( 'NONE', #743 ) ;
#7838=CARTESIAN_POINT ( 'NONE',  ( 17.00000000000000711, 277.8092731128509740, -29.71049682360898103 ) ) ;
#7879=CARTESIAN_POINT ( 'NONE',  ( 17.00000000000000000, 380.0000000000000000, -75.00000000000000000 ) ) ;
#7893=CARTESIAN_POINT ( 'NONE',  ( 65.00000000000000000, 0.000000000000000000, -7.000000000000006217 ) ) ;
#7904=ORIENTED_EDGE ( 'NONE', *, *, #2675, .F. ) ;
#7951=DIRECTION ( 'NONE',  ( -1.000000000000000000, -0.000000000000000000, -1.631319816340925608E-17 ) ) ;
#7959=CARTESIAN_POINT ( 'NONE',  ( 44.68009836720081296, 275.4439001176564830, 0.000000000000000000 ) ) ;
#7976=FACE_OUTER_BOUND ( 'NONE', #5590, .T. ) ;
#8029=LINE ( 'NONE', #13373, #2754 ) ;
#8037=CIRCLE ( 'NONE', #8314, 7.500000000000000000 ) ;
#8060=SURFACE_SIDE_STYLE ('',( #13654 ) ) ;
#8087=AXIS2_PLACEMENT_3D ( 'NONE', #5737, #9702, #8575 ) ;
#8172=( GEOMETRIC_REPRESENTATION_CONTEXT ( 3 ) GLOBAL_UNCERTAINTY_ASSIGNED_CONTEXT ( ( #183 ) ) GLOBAL_UNIT_ASSIGNED_CONTEXT ( ( #16217, #12355, #6842 ) ) REPRESENTATION_CONTEXT ( 'NONE', 'WORKASPACE' ) );
#8180=CARTESIAN_POINT ( 'NONE',  ( 75.00000000000000000, 0.000000000000000000, -7.000000000000006217 ) ) ;
#8191=PLANE ( 'NONE',  #1114 ) ;
#8210=ORIENTED_EDGE ( 'NONE', *, *, #3625, .T. ) ;
#8251=AXIS2_PLACEMENT_3D ( 'NONE', #3321, #15338, #11219 ) ;
#8314=AXIS2_PLACEMENT_3D ( 'NONE', #6719, #14809, #14724 ) ;
#8338=ADVANCED_FACE ( 'NONE', ( #8688 ), #12620, .F. ) ;
#8346=( GEOMETRIC_REPRESENTATION_CONTEXT ( 3 ) GLOBAL_UNCERTAINTY_ASSIGNED_CONTEXT ( ( #2744 ) ) GLOBAL_UNIT_ASSIGNED_CONTEXT ( ( #7740, #10340, #9046 ) ) REPRESENTATION_CONTEXT ( 'NONE', 'WORKASPACE' ) );
#8380=ORIENTED_EDGE ( 'NONE', *, *, #4766, .F. ) ;
#8413=FILL_AREA_STYLE ('',( #9351 ) ) ;
#8442=DIRECTION ( 'NONE',  ( 1.000000000000000000, 0.000000000000000000, 0.000000000000000000 ) ) ;
#8465=PLANE ( 'NONE',  #10952 ) ;
#8468=VERTEX_POINT ( 'NONE', #2997 ) ;
#8514=MANIFOLD_SOLID_BREP ( 'Cut-Extrude3', #1138 ) ;
#8517=FACE_OUTER_BOUND ( 'NONE', #2104, .T. ) ;
#8540=CIRCLE ( 'NONE', #4961, 9.999999999999994671 ) ;
#8575=DIRECTION ( 'NONE',  ( 1.000000000000000000, 0.000000000000000000, 0.000000000000000000 ) ) ;
#8587=ORIENTED_EDGE ( 'NONE', *, *, #16542, .F. ) ;
#8588=DIRECTION ( 'NONE',  ( 0.000000000000000000, -1.000000000000000000, 0.000000000000000000 ) ) ;
#8612=LINE ( 'NONE', #5943, #1761 ) ;
#8645=ORIENTED_EDGE ( 'NONE', *, *, #476, .T. ) ;
#8646=ORIENTED_EDGE ( 'NONE', *, *, #14435, .T. ) ;
#8688=FACE_OUTER_BOUND ( 'NONE', #4977, .T. ) ;
#8693=DIRECTION ( 'NONE',  ( 0.000000000000000000, 0.000000000000000000, 1.000000000000000000 ) ) ;
#8715=DIRECTION ( 'NONE',  ( -0.000000000000000000, -0.000000000000000000, 1.000000000000000000 ) ) ;
#8791=LINE ( 'NONE', #1205, #5825 ) ;
#8838=ORIENTED_EDGE ( 'NONE', *, *, #13509, .F. ) ;
#8871=VECTOR ( 'NONE', #3329, 1000.000000000000000 ) ;
#8954=ORIENTED_EDGE ( 'NONE', *, *, #6023, .F. ) ;
#8961=ORIENTED_EDGE ( 'NONE', *, *, #7184, .T. ) ;
#8982=ORIENTED_EDGE ( 'NONE', *, *, #14435, .F. ) ;
#8986=DIRECTION ( 'NONE',  ( 0.000000000000000000, -1.000000000000000000, 0.000000000000000000 ) ) ;
#9046=( NAMED_UNIT ( * ) SI_UNIT ( $, .STERADIAN. ) SOLID_ANGLE_UNIT ( ) );
#9136=VECTOR ( 'NONE', #3948, 1000.000000000000000 ) ;
#9151=EDGE_LOOP ( 'NONE', ( #12898, #2397, #7705, #3666, #14196, #552, #4552, #3 ) ) ;
#9165=FACE_BOUND ( 'NONE', #11601, .T. ) ;
#9203=EDGE_CURVE ( 'NONE', #4345, #12485, #5490, .T. ) ;
#9254=VERTEX_POINT ( 'NONE', #12062 ) ;
#9264=CARTESIAN_POINT ( 'NONE',  ( 47.50000000000000000, 196.3050121726289206, -75.00000000000000000 ) ) ;
#9269=ADVANCED_FACE ( 'NONE', ( #301, #5518, #16004 ), #8191, .F. ) ;
#9270=CARTESIAN_POINT ( 'NONE',  ( -6.117449311278470645E-17, 355.3192028797624857, -29.71049682360898814 ) ) ;
#9351=FILL_AREA_STYLE_COLOUR ( '', #11734 ) ;
#9359=ORIENTED_EDGE ( 'NONE', *, *, #12907, .T. ) ;
#9381=EDGE_CURVE ( 'NONE', #9254, #6128, #16746, .T. ) ;
#9411=EDGE_CURVE ( 'NONE', #10513, #15829, #15917, .T. ) ;
#9463=VECTOR ( 'NONE', #344, 1000.000000000000000 ) ;
#9479=AXIS2_PLACEMENT_3D ( 'NONE', #6288, #16620, #7751 ) ;
#9490=DIRECTION ( 'NONE',  ( -1.000000000000000000, 0.000000000000000000, -0.000000000000000000 ) ) ;
#9524=VERTEX_POINT ( 'NONE', #10540 ) ;
#9525=CARTESIAN_POINT ( 'NONE',  ( 37.18009836720079875, 352.3758082234937206, 0.000000000000000000 ) ) ;
#9536=DIRECTION ( 'NONE',  ( 0.000000000000000000, 0.000000000000000000, 1.000000000000000000 ) ) ;
#9627=DIRECTION ( 'NONE',  ( -1.803905316987902281E-16, 1.000000000000000000, 0.000000000000000000 ) ) ;
#9630=EDGE_CURVE ( 'NONE', #976, #16546, #580, .T. ) ;
#9652=DIRECTION ( 'NONE',  ( 0.000000000000000000, 0.000000000000000000, -1.000000000000000000 ) ) ;
#9677=FACE_OUTER_BOUND ( 'NONE', #3979, .T. ) ;
#9681=CARTESIAN_POINT ( 'NONE',  ( 65.00000000000000000, 380.0000000000000000, -7.000000000000006217 ) ) ;
#9692=CARTESIAN_POINT ( 'NONE',  ( 27.49999999999999645, 196.3050121726289206, -17.00000000000000000 ) ) ;
#9700=LINE ( 'NONE', #1701, #12387 ) ;
#9702=DIRECTION ( 'NONE',  ( 0.000000000000000000, 0.000000000000000000, 1.000000000000000000 ) ) ;
#9706=DIRECTION ( 'NONE',  ( 0.000000000000000000, 0.000000000000000000, -1.000000000000000000 ) ) ;
#9725=VERTEX_POINT ( 'NONE', #9692 ) ;
#9729=EDGE_CURVE ( 'NONE', #15829, #5489, #5643, .T. ) ;
#9791=VECTOR ( 'NONE', #10112, 1000.000000000000000 ) ;
#9802=VECTOR ( 'NONE', #2907, 1000.000000000000000 ) ;
#9819=VERTEX_POINT ( 'NONE', #6135 ) ;
#9827=EDGE_CURVE ( 'NONE', #377, #14070, #12764, .T. ) ;
#9839=DIRECTION ( 'NONE',  ( -1.000000000000000000, 0.000000000000000000, -1.631319816340925608E-17 ) ) ;
#9841=ADVANCED_FACE ( 'NONE', ( #13967 ), #16623, .F. ) ;
#9894=PLANE ( 'NONE',  #3418 ) ;
#9896=VECTOR ( 'NONE', #2583, 1000.000000000000000 ) ;
#9902=ORIENTED_EDGE ( 'NONE', *, *, #2080, .T. ) ;
#9912=EDGE_CURVE ( 'NONE', #377, #4587, #8540, .T. ) ;
#9913=EDGE_CURVE ( 'NONE', #976, #377, #1413, .T. ) ;
#9984=CARTESIAN_POINT ( 'NONE',  ( 37.50000000000000000, 196.3050121726289206, -75.00000000000000000 ) ) ;
#9986=ORIENTED_EDGE ( 'NONE', *, *, #11191, .T. ) ;
#10026=CARTESIAN_POINT ( 'NONE',  ( 0.000000000000000000, 0.000000000000000000, 0.000000000000000000 ) ) ;
#10034=DIRECTION ( 'NONE',  ( -0.000000000000000000, -1.000000000000000000, -0.000000000000000000 ) ) ;
#10100=AXIS2_PLACEMENT_3D ( 'NONE', #4218, #3013, #13333 ) ;
#10110=DIRECTION ( 'NONE',  ( -1.000000000000000000, -0.000000000000000000, -1.631319816340925608E-17 ) ) ;
#10112=DIRECTION ( 'NONE',  ( -1.000000000000000000, -0.000000000000000000, -0.000000000000000000 ) ) ;
#10139=VECTOR ( 'NONE', #2070, 1000.000000000000000 ) ;
#10140=SHAPE_REPRESENTATION_RELATIONSHIP ( 'NONE' , 'NONE' ,  #1329, #15527 ) ;
#10185=DIRECTION ( 'NONE',  ( -0.000000000000000000, 1.000000000000000000, -0.000000000000000000 ) ) ;
#10220=DIRECTION ( 'NONE',  ( 0.000000000000000000, 0.000000000000000000, 1.000000000000000000 ) ) ;
#10281=LINE ( 'NONE', #16700, #15451 ) ;
#10328=ORIENTED_EDGE ( 'NONE', *, *, #1227, .F. ) ;
#10340=( NAMED_UNIT ( * ) PLANE_ANGLE_UNIT ( ) SI_UNIT ( $, .RADIAN. ) );
#10366=LINE ( 'NONE', #1083, #2190 ) ;
#10375=LINE ( 'NONE', #6154, #16329 ) ;
#10405=ORIENTED_EDGE ( 'NONE', *, *, #13509, .T. ) ;
#10419=ORIENTED_EDGE ( 'NONE', *, *, #3018, .F. ) ;
#10421=CARTESIAN_POINT ( 'NONE',  ( 17.00000000000000000, 380.0000000000000000, -75.00000000000000000 ) ) ;
#10434=DIRECTION ( 'NONE',  ( 1.000000000000000000, 0.000000000000000000, 0.000000000000000000 ) ) ;
#10437=CARTESIAN_POINT ( 'NONE',  ( 29.68009836720079875, 380.0000000000000000, -17.00000000000000355 ) ) ;
#10458=LINE ( 'NONE', #12699, #16792 ) ;
#10463=CARTESIAN_POINT ( 'NONE',  ( 44.68009836720079875, 352.3758082234937206, -75.00000000000000000 ) ) ;
#10512=DIRECTION ( 'NONE',  ( -0.000000000000000000, -0.000000000000000000, 1.000000000000000000 ) ) ;
#10513=VERTEX_POINT ( 'NONE', #461 ) ;
#10524=VECTOR ( 'NONE', #10034, 1000.000000000000000 ) ;
#10532=DIRECTION ( 'NONE',  ( 1.000000000000000000, 0.000000000000000000, -0.000000000000000000 ) ) ;
#10540=CARTESIAN_POINT ( 'NONE',  ( 47.50000000000000000, 196.3050121726289206, 0.000000000000000000 ) ) ;
#10560=ORIENTED_EDGE ( 'NONE', *, *, #13997, .T. ) ;
#10561=CARTESIAN_POINT ( 'NONE',  ( 17.00000000000000000, 0.000000000000000000, -65.00000000000000000 ) ) ;
#10631=MECHANICAL_DESIGN_GEOMETRIC_PRESENTATION_REPRESENTATION('',(#5139),#8172);
#10653=DIRECTION ( 'NONE',  ( -1.631319816340925608E-17, 0.000000000000000000, 1.000000000000000000 ) ) ;
#10661=ADVANCED_FACE ( 'NONE', ( #8517 ), #5853, .T. ) ;
#10707=CARTESIAN_POINT ( 'NONE',  ( 75.00000000000000000, 380.0000000000000000, -7.000000000000006217 ) ) ;
#10744=ORIENTED_EDGE ( 'NONE', *, *, #11937, .T. ) ;
#10762=ORIENTED_EDGE ( 'NONE', *, *, #16418, .T. ) ;
#10771=DIRECTION ( 'NONE',  ( -1.000000000000000000, -0.000000000000000000, -1.631319816340925608E-17 ) ) ;
#10782=AXIS2_PLACEMENT_3D ( 'NONE', #5020, #11726, #10434 ) ;
#10838=AXIS2_PLACEMENT_3D ( 'NONE', #3699, #6251, #10220 ) ;
#10886=AXIS2_PLACEMENT_3D ( 'NONE', #13375, #16111, #5451 ) ;
#10889=DIRECTION ( 'NONE',  ( -0.000000000000000000, 1.000000000000000000, -0.000000000000000000 ) ) ;
#10952=AXIS2_PLACEMENT_3D ( 'NONE', #15069, #12495, #9839 ) ;
#10966=ADVANCED_FACE ( 'NONE', ( #12204 ), #13492, .T. ) ;
#10984=EDGE_CURVE ( 'NONE', #9254, #1629, #4625, .T. ) ;
#10987=CARTESIAN_POINT ( 'NONE',  ( 75.00000000000000000, 380.0000000000000000, 0.000000000000000000 ) ) ;
#11049=ADVANCED_FACE ( 'NONE', ( #16473 ), #3515, .T. ) ;
#11096=LINE ( 'NONE', #11177, #4104 ) ;
#11105=EDGE_CURVE ( 'NONE', #8468, #13435, #3263, .T. ) ;
#11132=ORIENTED_EDGE ( 'NONE', *, *, #9381, .F. ) ;
#11145=EDGE_LOOP ( 'NONE', ( #1990, #15336, #6878, #8210 ) ) ;
#11161=CARTESIAN_POINT ( 'NONE',  ( 29.68009836720079875, 352.3758082234937206, -75.00000000000000000 ) ) ;
#11177=CARTESIAN_POINT ( 'NONE',  ( 17.00000000000000711, 380.0000000000000000, -17.00000000000000355 ) ) ;
#11191=EDGE_CURVE ( 'NONE', #13435, #16667, #10458, .T. ) ;
#11219=DIRECTION ( 'NONE',  ( 1.000000000000000000, 0.000000000000000000, 0.000000000000000000 ) ) ;
#11361=EDGE_LOOP ( 'NONE', ( #1741, #10744, #1904, #15936 ) ) ;
#11384=EDGE_CURVE ( 'NONE', #3161, #13435, #1991, .T. ) ;
#11388=CARTESIAN_POINT ( 'NONE',  ( 1.223489862255693833E-15, 0.000000000000000000, -75.00000000000000000 ) ) ;
#11417=DIRECTION ( 'NONE',  ( -1.000000000000000000, -0.000000000000000000, -1.631319816340925608E-17 ) ) ;
#11443=ORIENTED_EDGE ( 'NONE', *, *, #13051, .T. ) ;
#11466=FACE_OUTER_BOUND ( 'NONE', #5970, .T. ) ;
#11479=CARTESIAN_POINT ( 'NONE',  ( 75.00000000000000000, 355.3192028797624857, -37.21049682360899169 ) ) ;
#11512=EDGE_CURVE ( 'NONE', #6709, #4587, #2176, .T. ) ;
#11568=VERTEX_POINT ( 'NONE', #6118 ) ;
#11598=ORIENTED_EDGE ( 'NONE', *, *, #16355, .T. ) ;
#11601=EDGE_LOOP ( 'NONE', ( #16297, #16593 ) ) ;
#11642=DIRECTION ( 'NONE',  ( 1.000000000000000000, 0.000000000000000000, 0.000000000000000000 ) ) ;
#11649=CARTESIAN_POINT ( 'NONE',  ( 75.00000000000000000, 380.0000000000000000, 0.000000000000000000 ) ) ;
#11726=DIRECTION ( 'NONE',  ( -0.000000000000000000, -0.000000000000000000, 1.000000000000000000 ) ) ;
#11734=COLOUR_RGB ( '', 0.72549020, 0.75294118, 0.79215686) ;
#11758=EDGE_LOOP ( 'NONE', ( #1909, #14189, #15557, #16925 ) ) ;
#11766=DIRECTION ( 'NONE',  ( 0.000000000000000000, 0.000000000000000000, -1.000000000000000000 ) ) ;
#11841=CARTESIAN_POINT ( 'NONE',  ( 37.50000000000000000, 196.3050121726289206, -17.00000000000000000 ) ) ;
#11843=VECTOR ( 'NONE', #7951, 1000.000000000000000 ) ;
#11892=DIRECTION ( 'NONE',  ( 1.000000000000000000, 0.000000000000000000, 0.000000000000000000 ) ) ;
#11910=CARTESIAN_POINT ( 'NONE',  ( 17.00000000000000711, 380.0000000000000000, -17.00000000000000355 ) ) ;
#11911=AXIS2_PLACEMENT_3D ( 'NONE', #9984, #4408, #8442 ) ;
#11929=VECTOR ( 'NONE', #9706, 1000.000000000000000 ) ;
#11937=EDGE_CURVE ( 'NONE', #16470, #10513, #8612, .T. ) ;
#11940=PRODUCT_DEFINITION_FORMATION_WITH_SPECIFIED_SOURCE ( 'ANY', '', #1513, .NOT_KNOWN. ) ;
#11946=DIRECTION ( 'NONE',  ( 0.000000000000000000, -0.000000000000000000, -1.000000000000000000 ) ) ;
#11951=FACE_OUTER_BOUND ( 'NONE', #16940, .T. ) ;
#11984=ORIENTED_EDGE ( 'NONE', *, *, #5056, .F. ) ;
#12017=SURFACE_STYLE_USAGE ( .BOTH. , #8060 ) ;
#12062=CARTESIAN_POINT ( 'NONE',  ( 44.68009836720081296, 275.4439001176564830, -17.00000000000000000 ) ) ;
#12066=ORIENTED_EDGE ( 'NONE', *, *, #6023, .T. ) ;
#12109=EDGE_LOOP ( 'NONE', ( #7335, #11984, #826, #3541 ) ) ;
#12186=EDGE_LOOP ( 'NONE', ( #16086, #2593, #13712, #15103 ) ) ;
#12204=FACE_OUTER_BOUND ( 'NONE', #15413, .T. ) ;
#12206=CARTESIAN_POINT ( 'NONE',  ( 44.68009836720079875, 352.3758082234937206, -75.00000000000000000 ) ) ;
#12290=LINE ( 'NONE', #16230, #6807 ) ;
#12300=ORIENTED_EDGE ( 'NONE', *, *, #9630, .F. ) ;
#12355=( NAMED_UNIT ( * ) PLANE_ANGLE_UNIT ( ) SI_UNIT ( $, .RADIAN. ) );
#12366=ORIENTED_EDGE ( 'NONE', *, *, #11105, .F. ) ;
#12378=SHAPE_DEFINITION_REPRESENTATION ( #6993, #1329 ) ;
#12386=DIRECTION ( 'NONE',  ( 0.000000000000000000, -1.000000000000000000, 0.000000000000000000 ) ) ;
#12387=VECTOR ( 'NONE', #4108, 1000.000000000000000 ) ;
#12403=CARTESIAN_POINT ( 'NONE',  ( 0.000000000000000000, 380.0000000000000000, 0.000000000000000000 ) ) ;
#12418=ORIENTED_EDGE ( 'NONE', *, *, #1998, .T. ) ;
#12427=LINE ( 'NONE', #669, #8871 ) ;
#12449=DIRECTION ( 'NONE',  ( 0.000000000000000000, 0.000000000000000000, -1.000000000000000000 ) ) ;
#12485=VERTEX_POINT ( 'NONE', #15538 ) ;
#12495=DIRECTION ( 'NONE',  ( 1.631319816340925608E-17, 0.000000000000000000, -1.000000000000000000 ) ) ;
#12544=DIRECTION ( 'NONE',  ( -1.000000000000000000, 0.000000000000000000, -0.000000000000000000 ) ) ;
#12547=AXIS2_PLACEMENT_3D ( 'NONE', #862, #3040, #15295 ) ;
#12593=CARTESIAN_POINT ( 'NONE',  ( 17.00000000000000355, 380.0000000000000000, -44.71049682360899169 ) ) ;
#12620=CYLINDRICAL_SURFACE ( 'NONE', #12547, 7.500000000000000000 ) ;
#12625=AXIS2_PLACEMENT_3D ( 'NONE', #4157, #10771, #6724 ) ;
#12628=PRODUCT_CONTEXT ( 'NONE', #16736, 'mechanical' ) ;
#12670=ORIENTED_EDGE ( 'NONE', *, *, #7184, .F. ) ;
#12692=CARTESIAN_POINT ( 'NONE',  ( 75.00000000000000000, 380.0000000000000000, 0.000000000000000000 ) ) ;
#12699=CARTESIAN_POINT ( 'NONE',  ( 29.68009836720079875, 352.3758082234937206, 0.000000000000000000 ) ) ;
#12726=DIRECTION ( 'NONE',  ( 0.000000000000000000, -1.000000000000000000, 0.000000000000000000 ) ) ;
#12764=LINE ( 'NONE', #11388, #3861 ) ;
#12772=DIRECTION ( 'NONE',  ( -0.000000000000000000, -1.000000000000000000, -0.000000000000000000 ) ) ;
#12785=AXIS2_PLACEMENT_3D ( 'NONE', #13101, #10512, #11892 ) ;
#12801=ORIENTED_EDGE ( 'NONE', *, *, #4465, .F. ) ;
#12835=FACE_BOUND ( 'NONE', #15509, .T. ) ;
#12838=ORIENTED_EDGE ( 'NONE', *, *, #16434, .F. ) ;
#12875=LINE ( 'NONE', #6326, #1707 ) ;
#12898=ORIENTED_EDGE ( 'NONE', *, *, #3326, .T. ) ;
#12901=AXIS2_PLACEMENT_3D ( 'NONE', #7893, #6510, #11766 ) ;
#12907=EDGE_CURVE ( 'NONE', #14070, #2365, #10366, .T. ) ;
#12911=DIRECTION ( 'NONE',  ( -1.000000000000000000, 0.000000000000000000, 1.196361017915039732E-16 ) ) ;
#12922=DIRECTION ( 'NONE',  ( 0.000000000000000000, -1.000000000000000000, 0.000000000000000000 ) ) ;
#12938=AXIS2_PLACEMENT_3D ( 'NONE', #13756, #12726, #4724 ) ;
#12976=EDGE_CURVE ( 'NONE', #9819, #3376, #6146, .T. ) ;
#13051=EDGE_CURVE ( 'NONE', #16546, #14070, #15764, .T. ) ;
#13059=CIRCLE ( 'NONE', #16341, 7.500000000000007105 ) ;
#13074=EDGE_CURVE ( 'NONE', #16546, #15577, #8029, .T. ) ;
#13101=CARTESIAN_POINT ( 'NONE',  ( 37.18009836720080585, 275.4439001176564830, 0.000000000000000000 ) ) ;
#13129=ORIENTED_EDGE ( 'NONE', *, *, #12907, .F. ) ;
#13193=ADVANCED_FACE ( 'NONE', ( #9677 ), #8465, .F. ) ;
#13230=ORIENTED_EDGE ( 'NONE', *, *, #5056, .T. ) ;
#13231=CARTESIAN_POINT ( 'NONE',  ( 0.000000000000000000, 0.000000000000000000, 0.000000000000000000 ) ) ;
#13247=EDGE_LOOP ( 'NONE', ( #14144, #5302, #8380, #10405 ) ) ;
#13298=CARTESIAN_POINT ( 'NONE',  ( 17.00000000000000711, 355.3192028797624857, -37.21049682360899169 ) ) ;
#13333=DIRECTION ( 'NONE',  ( 0.000000000000000000, 0.000000000000000000, 1.000000000000000000 ) ) ;
#13373=CARTESIAN_POINT ( 'NONE',  ( 0.000000000000000000, 380.0000000000000000, 0.000000000000000000 ) ) ;
#13375=CARTESIAN_POINT ( 'NONE',  ( 1.223489862255693833E-15, 380.0000000000000000, -75.00000000000000000 ) ) ;
#13435=VERTEX_POINT ( 'NONE', #15040 ) ;
#13457=EDGE_CURVE ( 'NONE', #16470, #1459, #11096, .T. ) ;
#13475=DIRECTION ( 'NONE',  ( -0.000000000000000000, -0.000000000000000000, 1.000000000000000000 ) ) ;
#13492=PLANE ( 'NONE',  #4452 ) ;
#13493=LINE ( 'NONE', #10026, #6655 ) ;
#13509=EDGE_CURVE ( 'NONE', #478, #2521, #3364, .T. ) ;
#13514=CIRCLE ( 'NONE', #2518, 10.00000000000000178 ) ;
#13565=ORIENTED_EDGE ( 'NONE', *, *, #1998, .F. ) ;
#13573=LINE ( 'NONE', #10987, #11929 ) ;
#13582=EDGE_CURVE ( 'NONE', #882, #12485, #4303, .T. ) ;
#13596=ORIENTED_EDGE ( 'NONE', *, *, #5379, .T. ) ;
#13639=ORIENTED_EDGE ( 'NONE', *, *, #5379, .F. ) ;
#13647=FACE_BOUND ( 'NONE', #3940, .T. ) ;
#13654=SURFACE_STYLE_FILL_AREA ( #8413 ) ;
#13712=ORIENTED_EDGE ( 'NONE', *, *, #16542, .T. ) ;
#13725=CARTESIAN_POINT ( 'NONE',  ( 0.000000000000000000, 380.0000000000000000, 0.000000000000000000 ) ) ;
#13756=CARTESIAN_POINT ( 'NONE',  ( 65.00000000000000000, 380.0000000000000000, -7.000000000000006217 ) ) ;
#13783=CARTESIAN_POINT ( 'NONE',  ( 0.000000000000000000, 0.000000000000000000, 0.000000000000000000 ) ) ;
#13812=VECTOR ( 'NONE', #10185, 1000.000000000000000 ) ;
#13825=ORIENTED_EDGE ( 'NONE', *, *, #3446, .F. ) ;
#13845=DIRECTION ( 'NONE',  ( -1.000000000000000000, -0.000000000000000000, -0.000000000000000000 ) ) ;
#13872=DIRECTION ( 'NONE',  ( 5.551115123125781913E-15, 0.000000000000000000, -1.000000000000000000 ) ) ;
#13967=FACE_OUTER_BOUND ( 'NONE', #338, .T. ) ;
#13982=FACE_OUTER_BOUND ( 'NONE', #13247, .T. ) ;
#13997=EDGE_CURVE ( 'NONE', #5558, #11568, #16122, .T. ) ;
#14062=LINE ( 'NONE', #16880, #10524 ) ;
#14070=VERTEX_POINT ( 'NONE', #4531 ) ;
#14102=ORIENTED_EDGE ( 'NONE', *, *, #15169, .F. ) ;
#14143=CYLINDRICAL_SURFACE ( 'NONE', #10782, 10.00000000000000178 ) ;
#14144=ORIENTED_EDGE ( 'NONE', *, *, #1227, .T. ) ;
#14153=LINE ( 'NONE', #7677, #9791 ) ;
#14177=ORIENTED_EDGE ( 'NONE', *, *, #9913, .F. ) ;
#14182=AXIS2_PLACEMENT_3D ( 'NONE', #13725, #15178, #3414 ) ;
#14189=ORIENTED_EDGE ( 'NONE', *, *, #6138, .F. ) ;
#14196=ORIENTED_EDGE ( 'NONE', *, *, #15169, .T. ) ;
#14230=CARTESIAN_POINT ( 'NONE',  ( 7.000000000000001776, 0.000000000000000000, -75.00000000000000000 ) ) ;
#14232=FACE_OUTER_BOUND ( 'NONE', #12109, .T. ) ;
#14285=CARTESIAN_POINT ( 'NONE',  ( 75.00000000000000000, 0.000000000000000000, 0.000000000000000000 ) ) ;
#14313=VERTEX_POINT ( 'NONE', #3146 ) ;
#14387=VECTOR ( 'NONE', #7168, 1000.000000000000000 ) ;
#14402=AXIS2_PLACEMENT_3D ( 'NONE', #11841, #9536, #3000 ) ;
#14435=EDGE_CURVE ( 'NONE', #14313, #16667, #8791, .T. ) ;
#14666=DIRECTION ( 'NONE',  ( 0.000000000000000000, 0.000000000000000000, 1.000000000000000000 ) ) ;
#14682=CARTESIAN_POINT ( 'NONE',  ( 17.00000000000000711, 380.0000000000000000, -29.71049682360898814 ) ) ;
#14724=DIRECTION ( 'NONE',  ( 1.000000000000000000, 0.000000000000000000, 0.000000000000000000 ) ) ;
#14740=AXIS2_PLACEMENT_3D ( 'NONE', #9681, #3155, #13872 ) ;
#14809=DIRECTION ( 'NONE',  ( 0.000000000000000000, 0.000000000000000000, 1.000000000000000000 ) ) ;
#14827=FACE_OUTER_BOUND ( 'NONE', #1220, .T. ) ;
#14836=CARTESIAN_POINT ( 'NONE',  ( 75.00000000000000000, 355.3192028797624857, -44.71049682360899169 ) ) ;
#14896=CARTESIAN_POINT ( 'NONE',  ( 37.18009836720080585, 275.4439001176564830, -17.00000000000000000 ) ) ;
#14992=CARTESIAN_POINT ( 'NONE',  ( 44.68009836720079875, 352.3758082234937206, -17.00000000000000000 ) ) ;
#15013=PLANE ( 'NONE',  #14182 ) ;
#15040=CARTESIAN_POINT ( 'NONE',  ( 29.68009836720079875, 352.3758082234937206, 0.000000000000000000 ) ) ;
#15069=CARTESIAN_POINT ( 'NONE',  ( 75.00000000000000000, 355.3192028797624857, -44.71049682360899169 ) ) ;
#15103=ORIENTED_EDGE ( 'NONE', *, *, #5560, .T. ) ;
#15129=VERTEX_POINT ( 'NONE', #7340 ) ;
#15165=ADVANCED_FACE ( 'NONE', ( #11466 ), #14143, .F. ) ;
#15169=EDGE_CURVE ( 'NONE', #15577, #478, #10281, .T. ) ;
#15178=DIRECTION ( 'NONE',  ( 1.000000000000000000, -0.000000000000000000, 1.631319816340925608E-17 ) ) ;
#15200=DIRECTION ( 'NONE',  ( -1.803905316987902527E-16, 1.000000000000000000, 0.000000000000000000 ) ) ;
#15209=CARTESIAN_POINT ( 'NONE',  ( 44.68009836720079875, 352.3758082234937206, 0.000000000000000000 ) ) ;
#15217=DIRECTION ( 'NONE',  ( 1.000000000000000000, 0.000000000000000000, 0.000000000000000000 ) ) ;
#15224=EDGE_LOOP ( 'NONE', ( #1078, #15907, #1430, #13639 ) ) ;
#15230=EDGE_CURVE ( 'NONE', #4587, #3093, #47, .T. ) ;
#15232=ORIENTED_EDGE ( 'NONE', *, *, #9729, .F. ) ;
#15262=VECTOR ( 'NONE', #6756, 1000.000000000000000 ) ;
#15281=CARTESIAN_POINT ( 'NONE',  ( 44.68009836720079875, 380.0000000000000000, -17.00000000000000355 ) ) ;
#15295=DIRECTION ( 'NONE',  ( 1.000000000000000000, 0.000000000000000000, 0.000000000000000000 ) ) ;
#15336=ORIENTED_EDGE ( 'NONE', *, *, #15230, .T. ) ;
#15338=DIRECTION ( 'NONE',  ( -0.000000000000000000, -0.000000000000000000, 1.000000000000000000 ) ) ;
#15413=EDGE_LOOP ( 'NONE', ( #1246, #16906, #368, #3359, #1571, #10328, #5954, #13129 ) ) ;
#15430=DIRECTION ( 'NONE',  ( -1.000000000000000000, 0.000000000000000000, 0.000000000000000000 ) ) ;
#15451=VECTOR ( 'NONE', #11642, 1000.000000000000000 ) ;
#15509=EDGE_LOOP ( 'NONE', ( #7796, #13230, #16621, #2408 ) ) ;
#15515=CARTESIAN_POINT ( 'NONE',  ( 7.000000000000001776, 0.000000000000000000, -65.00000000000000000 ) ) ;
#15527=ADVANCED_BREP_SHAPE_REPRESENTATION ( '', ( #8514, #1488 ), #8346 ) ;
#15538=CARTESIAN_POINT ( 'NONE',  ( -6.117449311278464482E-17, 277.8092731128509740, -29.71049682360898103 ) ) ;
#15557=ORIENTED_EDGE ( 'NONE', *, *, #13582, .T. ) ;
#15577=VERTEX_POINT ( 'NONE', #12403 ) ;
#15605=DIRECTION ( 'NONE',  ( -0.000000000000000000, 1.000000000000000000, -8.952264470854156086E-17 ) ) ;
#15638=ORIENTED_EDGE ( 'NONE', *, *, #9203, .T. ) ;
#15668=DIRECTION ( 'NONE',  ( 0.000000000000000000, -1.000000000000000000, 0.000000000000000000 ) ) ;
#15764=LINE ( 'NONE', #6558, #1898 ) ;
#15806=ORIENTED_EDGE ( 'NONE', *, *, #9381, .T. ) ;
#15829=VERTEX_POINT ( 'NONE', #8180 ) ;
#15845=ORIENTED_EDGE ( 'NONE', *, *, #3018, .T. ) ;
#15869=ADVANCED_FACE ( 'NONE', ( #16251 ), #7305, .F. ) ;
#15907=ORIENTED_EDGE ( 'NONE', *, *, #11384, .F. ) ;
#15917=CIRCLE ( 'NONE', #12901, 10.00000000000000178 ) ;
#15928=CARTESIAN_POINT ( 'NONE',  ( 29.68009836720079875, 275.4439001176564830, 0.000000000000000000 ) ) ;
#15936=ORIENTED_EDGE ( 'NONE', *, *, #3625, .F. ) ;
#15966=ADVANCED_FACE ( 'NONE', ( #5854 ), #9894, .F. ) ;
#16004=FACE_OUTER_BOUND ( 'NONE', #7542, .T. ) ;
#16008=CARTESIAN_POINT ( 'NONE',  ( 75.00000000000000000, 380.0000000000000000, -7.000000000000006217 ) ) ;
#16063=CARTESIAN_POINT ( 'NONE',  ( 0.000000000000000000, 355.3192028797624857, -44.71049682360899169 ) ) ;
#16086=ORIENTED_EDGE ( 'NONE', *, *, #10984, .T. ) ;
#16109=DIRECTION ( 'NONE',  ( -1.631319816340925300E-17, -0.000000000000000000, 1.000000000000000000 ) ) ;
#16111=DIRECTION ( 'NONE',  ( 0.000000000000000000, 0.000000000000000000, 1.000000000000000000 ) ) ;
#16122=LINE ( 'NONE', #14836, #11843 ) ;
#16217=( LENGTH_UNIT ( ) NAMED_UNIT ( * ) SI_UNIT ( .MILLI., .METRE. ) );
#16230=CARTESIAN_POINT ( 'NONE',  ( 0.000000000000000000, 380.0000000000000000, 0.000000000000000000 ) ) ;
#16251=FACE_OUTER_BOUND ( 'NONE', #4167, .T. ) ;
#16297=ORIENTED_EDGE ( 'NONE', *, *, #3446, .T. ) ;
#16298=CIRCLE ( 'NONE', #6400, 10.00000000000000178 ) ;
#16306=AXIS2_PLACEMENT_3D ( 'NONE', #7296, #12544, #4718 ) ;
#16329=VECTOR ( 'NONE', #15605, 1000.000000000000000 ) ;
#16339=DIRECTION ( 'NONE',  ( 0.000000000000000000, -0.000000000000000000, -1.000000000000000000 ) ) ;
#16341=AXIS2_PLACEMENT_3D ( 'NONE', #14896, #1763, #475 ) ;
#16355=EDGE_CURVE ( 'NONE', #11568, #4345, #7260, .T. ) ;
#16382=ORIENTED_EDGE ( 'NONE', *, *, #11937, .F. ) ;
#16392=EDGE_LOOP ( 'NONE', ( #8982, #8587, #39, #9986 ) ) ;
#16399=ORIENTED_EDGE ( 'NONE', *, *, #1854, .F. ) ;
#16418=EDGE_CURVE ( 'NONE', #2365, #2521, #13493, .T. ) ;
#16434=EDGE_CURVE ( 'NONE', #5558, #5021, #2113, .T. ) ;
#16440=EDGE_CURVE ( 'NONE', #9725, #15129, #12427, .T. ) ;
#16470=VERTEX_POINT ( 'NONE', #5185 ) ;
#16473=FACE_OUTER_BOUND ( 'NONE', #2961, .T. ) ;
#16542=EDGE_CURVE ( 'NONE', #8468, #14313, #1081, .T. ) ;
#16543=DIRECTION ( 'NONE',  ( 1.000000000000000000, 0.000000000000000000, 0.000000000000000000 ) ) ;
#16546=VERTEX_POINT ( 'NONE', #6297 ) ;
#16593=ORIENTED_EDGE ( 'NONE', *, *, #4584, .T. ) ;
#16620=DIRECTION ( 'NONE',  ( -1.631319816340925608E-17, 8.952264470854156086E-17, 1.000000000000000000 ) ) ;
#16621=ORIENTED_EDGE ( 'NONE', *, *, #16434, .T. ) ;
#16623=CYLINDRICAL_SURFACE ( 'NONE', #8251, 7.500000000000007105 ) ;
#16667=VERTEX_POINT ( 'NONE', #15928 ) ;
#16700=CARTESIAN_POINT ( 'NONE',  ( 0.000000000000000000, 380.0000000000000000, 0.000000000000000000 ) ) ;
#16711=DIRECTION ( 'NONE',  ( -1.000000000000000000, -0.000000000000000000, -1.631319816340925608E-17 ) ) ;
#16736=APPLICATION_CONTEXT ( 'automotive_design' ) ;
#16746=LINE ( 'NONE', #1374, #9896 ) ;
#16771=PLANE ( 'NONE',  #7211 ) ;
#16792=VECTOR ( 'NONE', #940, 1000.000000000000000 ) ;
#16824=AXIS2_PLACEMENT_3D ( 'NONE', #11479, #16711, #4944 ) ;
#16880=CARTESIAN_POINT ( 'NONE',  ( 17.00000000000000711, 380.0000000000000000, -17.00000000000000355 ) ) ;
#16906=ORIENTED_EDGE ( 'NONE', *, *, #9912, .T. ) ;
#16925=ORIENTED_EDGE ( 'NONE', *, *, #4793, .T. ) ;
#16940=EDGE_LOOP ( 'NONE', ( #2530, #12801, #9902, #15638 ) ) ;
ENDSEC;
END-ISO-10303-21;
